ISO-10303-21;
HEADER;
/* Generated by software containing ST-Developer
 * from STEP Tools, Inc. (www.steptools.com) 
 */

FILE_DESCRIPTION(
/* description */ ('Hand-crank flanged shaft unit'),
/* implementation_level */ '2;1');

FILE_NAME(
/* name */ 'Flange bolt sleeve (5).step',
/* time_stamp */ '2026-10-27T18:35:45-07:00',
/* author */ (''),
/* organization */ (''),
/* preprocessor_version */ 'ST-DEVELOPER v20.2',
/* originating_system */ 'Autodesk Translation Framework v15.17.0.0',
/* authorisation */ '');

FILE_SCHEMA (('AUTOMOTIVE_DESIGN { 1 0 10303 214 3 1 1 }'));
ENDSEC;

DATA;
#10=MECHANICAL_DESIGN_GEOMETRIC_PRESENTATION_REPRESENTATION('',(#285),#6805);
#245=SHAPE_REPRESENTATION_RELATIONSHIP('SRR','None',#6906,#265);
#265=ADVANCED_BREP_SHAPE_REPRESENTATION('',(#306),#6789);
#285=STYLED_ITEM('',(#7098),#306);
#306=MANIFOLD_SOLID_BREP('Body1',#3326);
#352=FACE_BOUND('',#784,.T.);
#353=FACE_BOUND('',#786,.T.);
#436=PLANE('',#3653);
#437=PLANE('',#3654);
#561=FACE_OUTER_BOUND('',#781,.T.);
#562=FACE_OUTER_BOUND('',#782,.T.);
#563=FACE_OUTER_BOUND('',#783,.T.);
#564=FACE_OUTER_BOUND('',#785,.T.);
#781=EDGE_LOOP('',(#2443,#2444,#2445,#2446));
#782=EDGE_LOOP('',(#2447,#2448,#2449,#2450));
#783=EDGE_LOOP('',(#2451));
#784=EDGE_LOOP('',(#2452));
#785=EDGE_LOOP('',(#2453));
#786=EDGE_LOOP('',(#2454));
#1037=LINE('',#5151,#1265);
#1038=LINE('',#5157,#1266);
#1265=VECTOR('',#4186,0.425);
#1266=VECTOR('',#4193,0.595);
#1477=CIRCLE('',#3648,0.425);
#1478=CIRCLE('',#3649,0.425);
#1479=CIRCLE('',#3651,0.595);
#1480=CIRCLE('',#3652,0.595);
#1633=VERTEX_POINT('',#5148);
#1634=VERTEX_POINT('',#5150);
#1635=VERTEX_POINT('',#5154);
#1636=VERTEX_POINT('',#5156);
#1939=EDGE_CURVE('',#1633,#1633,#1477,.T.);
#1940=EDGE_CURVE('',#1633,#1634,#1037,.T.);
#1941=EDGE_CURVE('',#1634,#1634,#1478,.T.);
#1942=EDGE_CURVE('',#1635,#1635,#1479,.T.);
#1943=EDGE_CURVE('',#1635,#1636,#1038,.T.);
#1944=EDGE_CURVE('',#1636,#1636,#1480,.T.);
#2443=ORIENTED_EDGE('',*,*,#1939,.F.);
#2444=ORIENTED_EDGE('',*,*,#1940,.T.);
#2445=ORIENTED_EDGE('',*,*,#1941,.T.);
#2446=ORIENTED_EDGE('',*,*,#1940,.F.);
#2447=ORIENTED_EDGE('',*,*,#1942,.F.);
#2448=ORIENTED_EDGE('',*,*,#1943,.T.);
#2449=ORIENTED_EDGE('',*,*,#1944,.T.);
#2450=ORIENTED_EDGE('',*,*,#1943,.F.);
#2451=ORIENTED_EDGE('',*,*,#1942,.T.);
#2452=ORIENTED_EDGE('',*,*,#1939,.T.);
#2453=ORIENTED_EDGE('',*,*,#1944,.F.);
#2454=ORIENTED_EDGE('',*,*,#1941,.F.);
#3087=CYLINDRICAL_SURFACE('',#3647,0.425);
#3088=CYLINDRICAL_SURFACE('',#3650,0.595);
#3178=ADVANCED_FACE('',(#561),#3087,.F.);
#3179=ADVANCED_FACE('',(#562),#3088,.T.);
#3180=ADVANCED_FACE('',(#563,#352),#436,.T.);
#3181=ADVANCED_FACE('',(#564,#353),#437,.F.);
#3326=CLOSED_SHELL('',(#3178,#3179,#3180,#3181));
#3646=AXIS2_PLACEMENT_3D('',#5146,#4180,#4181);
#3647=AXIS2_PLACEMENT_3D('',#5147,#4182,#4183);
#3648=AXIS2_PLACEMENT_3D('',#5149,#4184,#4185);
#3649=AXIS2_PLACEMENT_3D('',#5152,#4187,#4188);
#3650=AXIS2_PLACEMENT_3D('',#5153,#4189,#4190);
#3651=AXIS2_PLACEMENT_3D('',#5155,#4191,#4192);
#3652=AXIS2_PLACEMENT_3D('',#5158,#4194,#4195);
#3653=AXIS2_PLACEMENT_3D('',#5159,#4196,#4197);
#3654=AXIS2_PLACEMENT_3D('',#5160,#4198,#4199);
#4180=DIRECTION('axis',(0.,0.,1.));
#4181=DIRECTION('refdir',(1.,0.,0.));
#4182=DIRECTION('center_axis',(0.,1.,0.));
#4183=DIRECTION('ref_axis',(1.,0.,0.));
#4184=DIRECTION('center_axis',(0.,-1.,0.));
#4185=DIRECTION('ref_axis',(1.,0.,0.));
#4186=DIRECTION('',(0.,-1.,0.));
#4187=DIRECTION('center_axis',(0.,-1.,0.));
#4188=DIRECTION('ref_axis',(1.,0.,0.));
#4189=DIRECTION('center_axis',(0.,1.,0.));
#4190=DIRECTION('ref_axis',(1.,0.,0.));
#4191=DIRECTION('center_axis',(0.,1.,0.));
#4192=DIRECTION('ref_axis',(1.,0.,0.));
#4193=DIRECTION('',(0.,-1.,0.));
#4194=DIRECTION('center_axis',(0.,1.,0.));
#4195=DIRECTION('ref_axis',(1.,0.,0.));
#4196=DIRECTION('center_axis',(0.,1.,0.));
#4197=DIRECTION('ref_axis',(1.,0.,0.));
#4198=DIRECTION('center_axis',(0.,1.,0.));
#4199=DIRECTION('ref_axis',(1.,0.,0.));
#5146=CARTESIAN_POINT('',(0.,0.,0.));
#5147=CARTESIAN_POINT('Origin',(-3.2,21.,10.7));
#5148=CARTESIAN_POINT('',(-3.625,22.,10.7));
#5149=CARTESIAN_POINT('Origin',(-3.2,22.,10.7));
#5150=CARTESIAN_POINT('',(-3.625,21.,10.7));
#5151=CARTESIAN_POINT('',(-3.625,21.,10.7));
#5152=CARTESIAN_POINT('Origin',(-3.2,21.,10.7));
#5153=CARTESIAN_POINT('Origin',(-3.2,21.,10.7));
#5154=CARTESIAN_POINT('',(-3.795,22.,10.7));
#5155=CARTESIAN_POINT('Origin',(-3.2,22.,10.7));
#5156=CARTESIAN_POINT('',(-3.795,21.,10.7));
#5157=CARTESIAN_POINT('',(-3.795,21.,10.7));
#5158=CARTESIAN_POINT('Origin',(-3.2,21.,10.7));
#5159=CARTESIAN_POINT('Origin',(-3.2,22.,10.7));
#5160=CARTESIAN_POINT('Origin',(-3.2,21.,10.7));
#6764=UNCERTAINTY_MEASURE_WITH_UNIT(LENGTH_MEASURE(0.001),#6806,
'DISTANCE_ACCURACY_VALUE',
'Maximum model space distance between geometric entities at asserted c
onnectivities');
#6780=UNCERTAINTY_MEASURE_WITH_UNIT(LENGTH_MEASURE(0.001),#6806,
'DISTANCE_ACCURACY_VALUE',
'Maximum model space distance between geometric entities at asserted c
onnectivities');
#6789=(
GEOMETRIC_REPRESENTATION_CONTEXT(3)
GLOBAL_UNCERTAINTY_ASSIGNED_CONTEXT((#6764))
GLOBAL_UNIT_ASSIGNED_CONTEXT((#6806,#6808,#6809))
REPRESENTATION_CONTEXT('','3D')
);
#6805=(
GEOMETRIC_REPRESENTATION_CONTEXT(3)
GLOBAL_UNCERTAINTY_ASSIGNED_CONTEXT((#6780))
GLOBAL_UNIT_ASSIGNED_CONTEXT((#6806,#6808,#6809))
REPRESENTATION_CONTEXT('','3D')
);
#6806=(
LENGTH_UNIT()
NAMED_UNIT(*)
SI_UNIT(.CENTI.,.METRE.)
);
#6808=(
NAMED_UNIT(*)
PLANE_ANGLE_UNIT()
SI_UNIT($,.RADIAN.)
);
#6809=(
NAMED_UNIT(*)
SI_UNIT($,.STERADIAN.)
SOLID_ANGLE_UNIT()
);
#6818=SHAPE_DEFINITION_REPRESENTATION(#6842,#6906);
#6842=PRODUCT_DEFINITION_SHAPE('',$,#6931);
#6906=SHAPE_REPRESENTATION('',(#3646),#6789);
#6922=PRODUCT_DEFINITION_CONTEXT('part definition',#6996,'design');
#6931=PRODUCT_DEFINITION('Flange bolt sleeve (5)',
'Flange bolt sleeve (5)',#6955,#6922);
#6955=PRODUCT_DEFINITION_FORMATION('',$,#7006);
#6996=APPLICATION_CONTEXT(
'Core Data for Automotive Mechanical Design Process');
#6997=PRODUCT_CONTEXT('part definition',#6996,'mechanical');
#7006=PRODUCT('Flange bolt sleeve (5)','Flange bolt sleeve (5)',
'Flange bolt sleeve (5)',(#6997));
#7092=COLOUR_RGB('Black',0.12,0.14,0.17);
#7093=FILL_AREA_STYLE_COLOUR('',#7092);
#7094=FILL_AREA_STYLE('',(#7093));
#7095=SURFACE_STYLE_FILL_AREA(#7094);
#7096=SURFACE_SIDE_STYLE('',(#7095));
#7097=SURFACE_STYLE_USAGE(.BOTH.,#7096);
#7098=PRESENTATION_STYLE_ASSIGNMENT((#7097));
ENDSEC;
END-ISO-10303-21;
